ISO-10303-21;
HEADER;
/* Generated by software containing ST-Developer
 * from STEP Tools, Inc. (www.steptools.com) 
 */

FILE_DESCRIPTION(
/* description */ ('Compact intermittent indexer'),
/* implementation_level */ '2;1');

FILE_NAME(
/* name */ 'Cap Screw - M5x20.step',
/* time_stamp */ '2026-10-29T16:32:17-07:00',
/* author */ (''),
/* organization */ (''),
/* preprocessor_version */ 'ST-DEVELOPER v20.2',
/* originating_system */ 'Autodesk Translation Framework v15.17.0.0',
/* authorisation */ '');

FILE_SCHEMA (('AUTOMOTIVE_DESIGN { 1 0 10303 214 3 1 1 }'));
ENDSEC;

DATA;
#10=MECHANICAL_DESIGN_GEOMETRIC_PRESENTATION_REPRESENTATION('',(#262),#10837);
#193=ORIENTED_CLOSED_SHELL('',*,#5635,.F.);
#195=CONICAL_SURFACE('',#6165,0.4,0.785398163397448);
#196=CONICAL_SURFACE('',#6169,0.41,0.785398163397448);
#197=CONICAL_SURFACE('',#6173,0.26,0.463647609000806);
#198=CONICAL_SURFACE('',#6177,0.225,0.785398163397448);
#207=BREP_WITH_VOIDS('Body1',#5634,(#193));
#214=SHAPE_REPRESENTATION_RELATIONSHIP('SRR','None',#10948,#238);
#238=ADVANCED_BREP_SHAPE_REPRESENTATION('',(#207),#10815);
#262=STYLED_ITEM('',(#11173),#207);
#422=FACE_BOUND('',#1163,.T.);
#528=PLANE('',#6163);
#529=PLANE('',#6171);
#530=PLANE('',#6179);
#531=PLANE('',#6180);
#532=PLANE('',#6181);
#533=PLANE('',#6182);
#534=PLANE('',#6183);
#535=PLANE('',#6184);
#536=PLANE('',#6185);
#537=PLANE('',#6186);
#538=PLANE('',#6187);
#761=FACE_OUTER_BOUND('',#1158,.T.);
#762=FACE_OUTER_BOUND('',#1159,.T.);
#763=FACE_OUTER_BOUND('',#1160,.T.);
#764=FACE_OUTER_BOUND('',#1161,.T.);
#765=FACE_OUTER_BOUND('',#1162,.T.);
#766=FACE_OUTER_BOUND('',#1164,.T.);
#767=FACE_OUTER_BOUND('',#1165,.T.);
#768=FACE_OUTER_BOUND('',#1166,.T.);
#769=FACE_OUTER_BOUND('',#1167,.T.);
#770=FACE_OUTER_BOUND('',#1168,.T.);
#771=FACE_OUTER_BOUND('',#1169,.T.);
#772=FACE_OUTER_BOUND('',#1170,.T.);
#773=FACE_OUTER_BOUND('',#1171,.T.);
#774=FACE_OUTER_BOUND('',#1172,.T.);
#775=FACE_OUTER_BOUND('',#1173,.T.);
#776=FACE_OUTER_BOUND('',#1174,.T.);
#777=FACE_OUTER_BOUND('',#1175,.T.);
#1158=EDGE_LOOP('',(#4164));
#1159=EDGE_LOOP('',(#4165,#4166,#4167,#4168));
#1160=EDGE_LOOP('',(#4169,#4170,#4171,#4172));
#1161=EDGE_LOOP('',(#4173,#4174,#4175,#4176));
#1162=EDGE_LOOP('',(#4177));
#1163=EDGE_LOOP('',(#4178));
#1164=EDGE_LOOP('',(#4179,#4180,#4181,#4182));
#1165=EDGE_LOOP('',(#4183,#4184,#4185,#4186));
#1166=EDGE_LOOP('',(#4187,#4188,#4189,#4190));
#1167=EDGE_LOOP('',(#4191));
#1168=EDGE_LOOP('',(#4192,#4193,#4194,#4195));
#1169=EDGE_LOOP('',(#4196,#4197,#4198,#4199));
#1170=EDGE_LOOP('',(#4200,#4201,#4202,#4203));
#1171=EDGE_LOOP('',(#4204,#4205,#4206,#4207));
#1172=EDGE_LOOP('',(#4208,#4209,#4210,#4211));
#1173=EDGE_LOOP('',(#4212,#4213,#4214,#4215));
#1174=EDGE_LOOP('',(#4216,#4217,#4218,#4219,#4220,#4221));
#1175=EDGE_LOOP('',(#4222,#4223,#4224,#4225,#4226,#4227));
#1540=LINE('',#9069,#1898);
#1541=LINE('',#9073,#1899);
#1542=LINE('',#9077,#1900);
#1543=LINE('',#9084,#1901);
#1544=LINE('',#9088,#1902);
#1545=LINE('',#9092,#1903);
#1546=LINE('',#9097,#1904);
#1547=LINE('',#9099,#1905);
#1548=LINE('',#9101,#1906);
#1549=LINE('',#9102,#1907);
#1550=LINE('',#9105,#1908);
#1551=LINE('',#9107,#1909);
#1552=LINE('',#9108,#1910);
#1553=LINE('',#9111,#1911);
#1554=LINE('',#9113,#1912);
#1555=LINE('',#9114,#1913);
#1556=LINE('',#9117,#1914);
#1557=LINE('',#9119,#1915);
#1558=LINE('',#9120,#1916);
#1559=LINE('',#9123,#1917);
#1560=LINE('',#9125,#1918);
#1561=LINE('',#9126,#1919);
#1562=LINE('',#9128,#1920);
#1563=LINE('',#9129,#1921);
#1898=VECTOR('',#7252,0.4);
#1899=VECTOR('',#7257,0.425);
#1900=VECTOR('',#7262,0.41);
#1901=VECTOR('',#7271,0.26);
#1902=VECTOR('',#7276,0.25);
#1903=VECTOR('',#7281,0.225);
#1904=VECTOR('',#7286,1.);
#1905=VECTOR('',#7287,1.);
#1906=VECTOR('',#7288,1.);
#1907=VECTOR('',#7289,1.);
#1908=VECTOR('',#7292,1.);
#1909=VECTOR('',#7293,1.);
#1910=VECTOR('',#7294,1.);
#1911=VECTOR('',#7297,1.);
#1912=VECTOR('',#7298,1.);
#1913=VECTOR('',#7299,1.);
#1914=VECTOR('',#7302,1.);
#1915=VECTOR('',#7303,1.);
#1916=VECTOR('',#7304,1.);
#1917=VECTOR('',#7307,1.);
#1918=VECTOR('',#7308,1.);
#1919=VECTOR('',#7309,1.);
#1920=VECTOR('',#7312,1.);
#1921=VECTOR('',#7313,1.);
#2266=CIRCLE('',#6164,0.375);
#2267=CIRCLE('',#6166,0.425);
#2268=CIRCLE('',#6168,0.425);
#2269=CIRCLE('',#6170,0.395);
#2270=CIRCLE('',#6172,0.27);
#2271=CIRCLE('',#6174,0.24505);
#2272=CIRCLE('',#6176,0.24505);
#2273=CIRCLE('',#6178,0.2);
#2634=VERTEX_POINT('',#9064);
#2635=VERTEX_POINT('',#9067);
#2636=VERTEX_POINT('',#9071);
#2637=VERTEX_POINT('',#9075);
#2638=VERTEX_POINT('',#9079);
#2639=VERTEX_POINT('',#9082);
#2640=VERTEX_POINT('',#9086);
#2641=VERTEX_POINT('',#9090);
#2642=VERTEX_POINT('',#9095);
#2643=VERTEX_POINT('',#9096);
#2644=VERTEX_POINT('',#9098);
#2645=VERTEX_POINT('',#9100);
#2646=VERTEX_POINT('',#9104);
#2647=VERTEX_POINT('',#9106);
#2648=VERTEX_POINT('',#9110);
#2649=VERTEX_POINT('',#9112);
#2650=VERTEX_POINT('',#9116);
#2651=VERTEX_POINT('',#9118);
#2652=VERTEX_POINT('',#9122);
#2653=VERTEX_POINT('',#9124);
#3204=EDGE_CURVE('',#2634,#2634,#2266,.T.);
#3205=EDGE_CURVE('',#2635,#2635,#2267,.T.);
#3206=EDGE_CURVE('',#2635,#2634,#1540,.T.);
#3207=EDGE_CURVE('',#2636,#2636,#2268,.T.);
#3208=EDGE_CURVE('',#2636,#2635,#1541,.T.);
#3209=EDGE_CURVE('',#2637,#2637,#2269,.T.);
#3210=EDGE_CURVE('',#2637,#2636,#1542,.T.);
#3211=EDGE_CURVE('',#2638,#2638,#2270,.T.);
#3212=EDGE_CURVE('',#2639,#2639,#2271,.F.);
#3213=EDGE_CURVE('',#2639,#2638,#1543,.T.);
#3214=EDGE_CURVE('',#2640,#2640,#2272,.F.);
#3215=EDGE_CURVE('',#2640,#2639,#1544,.T.);
#3216=EDGE_CURVE('',#2641,#2641,#2273,.T.);
#3217=EDGE_CURVE('',#2641,#2640,#1545,.T.);
#3218=EDGE_CURVE('',#2642,#2643,#1546,.T.);
#3219=EDGE_CURVE('',#2643,#2644,#1547,.T.);
#3220=EDGE_CURVE('',#2644,#2645,#1548,.T.);
#3221=EDGE_CURVE('',#2642,#2645,#1549,.T.);
#3222=EDGE_CURVE('',#2643,#2646,#1550,.T.);
#3223=EDGE_CURVE('',#2646,#2647,#1551,.T.);
#3224=EDGE_CURVE('',#2647,#2644,#1552,.T.);
#3225=EDGE_CURVE('',#2646,#2648,#1553,.T.);
#3226=EDGE_CURVE('',#2648,#2649,#1554,.T.);
#3227=EDGE_CURVE('',#2649,#2647,#1555,.T.);
#3228=EDGE_CURVE('',#2648,#2650,#1556,.T.);
#3229=EDGE_CURVE('',#2650,#2651,#1557,.T.);
#3230=EDGE_CURVE('',#2651,#2649,#1558,.T.);
#3231=EDGE_CURVE('',#2650,#2652,#1559,.T.);
#3232=EDGE_CURVE('',#2652,#2653,#1560,.T.);
#3233=EDGE_CURVE('',#2653,#2651,#1561,.T.);
#3234=EDGE_CURVE('',#2652,#2642,#1562,.T.);
#3235=EDGE_CURVE('',#2645,#2653,#1563,.T.);
#4164=ORIENTED_EDGE('',*,*,#3204,.F.);
#4165=ORIENTED_EDGE('',*,*,#3205,.F.);
#4166=ORIENTED_EDGE('',*,*,#3206,.T.);
#4167=ORIENTED_EDGE('',*,*,#3204,.T.);
#4168=ORIENTED_EDGE('',*,*,#3206,.F.);
#4169=ORIENTED_EDGE('',*,*,#3207,.F.);
#4170=ORIENTED_EDGE('',*,*,#3208,.T.);
#4171=ORIENTED_EDGE('',*,*,#3205,.T.);
#4172=ORIENTED_EDGE('',*,*,#3208,.F.);
#4173=ORIENTED_EDGE('',*,*,#3209,.F.);
#4174=ORIENTED_EDGE('',*,*,#3210,.T.);
#4175=ORIENTED_EDGE('',*,*,#3207,.T.);
#4176=ORIENTED_EDGE('',*,*,#3210,.F.);
#4177=ORIENTED_EDGE('',*,*,#3209,.T.);
#4178=ORIENTED_EDGE('',*,*,#3211,.F.);
#4179=ORIENTED_EDGE('',*,*,#3212,.F.);
#4180=ORIENTED_EDGE('',*,*,#3213,.T.);
#4181=ORIENTED_EDGE('',*,*,#3211,.T.);
#4182=ORIENTED_EDGE('',*,*,#3213,.F.);
#4183=ORIENTED_EDGE('',*,*,#3214,.F.);
#4184=ORIENTED_EDGE('',*,*,#3215,.T.);
#4185=ORIENTED_EDGE('',*,*,#3212,.T.);
#4186=ORIENTED_EDGE('',*,*,#3215,.F.);
#4187=ORIENTED_EDGE('',*,*,#3216,.F.);
#4188=ORIENTED_EDGE('',*,*,#3217,.T.);
#4189=ORIENTED_EDGE('',*,*,#3214,.T.);
#4190=ORIENTED_EDGE('',*,*,#3217,.F.);
#4191=ORIENTED_EDGE('',*,*,#3216,.T.);
#4192=ORIENTED_EDGE('',*,*,#3218,.T.);
#4193=ORIENTED_EDGE('',*,*,#3219,.T.);
#4194=ORIENTED_EDGE('',*,*,#3220,.T.);
#4195=ORIENTED_EDGE('',*,*,#3221,.F.);
#4196=ORIENTED_EDGE('',*,*,#3222,.T.);
#4197=ORIENTED_EDGE('',*,*,#3223,.T.);
#4198=ORIENTED_EDGE('',*,*,#3224,.T.);
#4199=ORIENTED_EDGE('',*,*,#3219,.F.);
#4200=ORIENTED_EDGE('',*,*,#3225,.T.);
#4201=ORIENTED_EDGE('',*,*,#3226,.T.);
#4202=ORIENTED_EDGE('',*,*,#3227,.T.);
#4203=ORIENTED_EDGE('',*,*,#3223,.F.);
#4204=ORIENTED_EDGE('',*,*,#3228,.T.);
#4205=ORIENTED_EDGE('',*,*,#3229,.T.);
#4206=ORIENTED_EDGE('',*,*,#3230,.T.);
#4207=ORIENTED_EDGE('',*,*,#3226,.F.);
#4208=ORIENTED_EDGE('',*,*,#3231,.T.);
#4209=ORIENTED_EDGE('',*,*,#3232,.T.);
#4210=ORIENTED_EDGE('',*,*,#3233,.T.);
#4211=ORIENTED_EDGE('',*,*,#3229,.F.);
#4212=ORIENTED_EDGE('',*,*,#3234,.T.);
#4213=ORIENTED_EDGE('',*,*,#3221,.T.);
#4214=ORIENTED_EDGE('',*,*,#3235,.T.);
#4215=ORIENTED_EDGE('',*,*,#3232,.F.);
#4216=ORIENTED_EDGE('',*,*,#3234,.F.);
#4217=ORIENTED_EDGE('',*,*,#3231,.F.);
#4218=ORIENTED_EDGE('',*,*,#3228,.F.);
#4219=ORIENTED_EDGE('',*,*,#3225,.F.);
#4220=ORIENTED_EDGE('',*,*,#3222,.F.);
#4221=ORIENTED_EDGE('',*,*,#3218,.F.);
#4222=ORIENTED_EDGE('',*,*,#3235,.F.);
#4223=ORIENTED_EDGE('',*,*,#3220,.F.);
#4224=ORIENTED_EDGE('',*,*,#3224,.F.);
#4225=ORIENTED_EDGE('',*,*,#3227,.F.);
#4226=ORIENTED_EDGE('',*,*,#3230,.F.);
#4227=ORIENTED_EDGE('',*,*,#3233,.F.);
#5224=CYLINDRICAL_SURFACE('',#6167,0.425);
#5225=CYLINDRICAL_SURFACE('',#6175,0.24505);
#5404=ADVANCED_FACE('',(#761),#528,.T.);
#5405=ADVANCED_FACE('',(#762),#195,.T.);
#5406=ADVANCED_FACE('',(#763),#5224,.T.);
#5407=ADVANCED_FACE('',(#764),#196,.T.);
#5408=ADVANCED_FACE('',(#765,#422),#529,.T.);
#5409=ADVANCED_FACE('',(#766),#197,.T.);
#5410=ADVANCED_FACE('',(#767),#5225,.T.);
#5411=ADVANCED_FACE('',(#768),#198,.T.);
#5412=ADVANCED_FACE('',(#769),#530,.T.);
#5413=ADVANCED_FACE('',(#770),#531,.F.);
#5414=ADVANCED_FACE('',(#771),#532,.F.);
#5415=ADVANCED_FACE('',(#772),#533,.F.);
#5416=ADVANCED_FACE('',(#773),#534,.F.);
#5417=ADVANCED_FACE('',(#774),#535,.F.);
#5418=ADVANCED_FACE('',(#775),#536,.F.);
#5419=ADVANCED_FACE('',(#776),#537,.F.);
#5420=ADVANCED_FACE('',(#777),#538,.F.);
#5634=CLOSED_SHELL('',(#5404,#5405,#5406,#5407,#5408,#5409,#5410,#5411,
#5412));
#5635=CLOSED_SHELL('',(#5413,#5414,#5415,#5416,#5417,#5418,#5419,#5420));
#6162=AXIS2_PLACEMENT_3D('',#9062,#7242,#7243);
#6163=AXIS2_PLACEMENT_3D('',#9063,#7244,#7245);
#6164=AXIS2_PLACEMENT_3D('',#9065,#7246,#7247);
#6165=AXIS2_PLACEMENT_3D('',#9066,#7248,#7249);
#6166=AXIS2_PLACEMENT_3D('',#9068,#7250,#7251);
#6167=AXIS2_PLACEMENT_3D('',#9070,#7253,#7254);
#6168=AXIS2_PLACEMENT_3D('',#9072,#7255,#7256);
#6169=AXIS2_PLACEMENT_3D('',#9074,#7258,#7259);
#6170=AXIS2_PLACEMENT_3D('',#9076,#7260,#7261);
#6171=AXIS2_PLACEMENT_3D('',#9078,#7263,#7264);
#6172=AXIS2_PLACEMENT_3D('',#9080,#7265,#7266);
#6173=AXIS2_PLACEMENT_3D('',#9081,#7267,#7268);
#6174=AXIS2_PLACEMENT_3D('',#9083,#7269,#7270);
#6175=AXIS2_PLACEMENT_3D('',#9085,#7272,#7273);
#6176=AXIS2_PLACEMENT_3D('',#9087,#7274,#7275);
#6177=AXIS2_PLACEMENT_3D('',#9089,#7277,#7278);
#6178=AXIS2_PLACEMENT_3D('',#9091,#7279,#7280);
#6179=AXIS2_PLACEMENT_3D('',#9093,#7282,#7283);
#6180=AXIS2_PLACEMENT_3D('',#9094,#7284,#7285);
#6181=AXIS2_PLACEMENT_3D('',#9103,#7290,#7291);
#6182=AXIS2_PLACEMENT_3D('',#9109,#7295,#7296);
#6183=AXIS2_PLACEMENT_3D('',#9115,#7300,#7301);
#6184=AXIS2_PLACEMENT_3D('',#9121,#7305,#7306);
#6185=AXIS2_PLACEMENT_3D('',#9127,#7310,#7311);
#6186=AXIS2_PLACEMENT_3D('',#9130,#7314,#7315);
#6187=AXIS2_PLACEMENT_3D('',#9131,#7316,#7317);
#7242=DIRECTION('axis',(0.,0.,1.));
#7243=DIRECTION('refdir',(1.,0.,0.));
#7244=DIRECTION('center_axis',(0.,1.,0.));
#7245=DIRECTION('ref_axis',(0.,0.,1.));
#7246=DIRECTION('center_axis',(0.,-1.,0.));
#7247=DIRECTION('ref_axis',(1.,0.,0.));
#7248=DIRECTION('center_axis',(0.,-1.,0.));
#7249=DIRECTION('ref_axis',(1.,0.,0.));
#7250=DIRECTION('center_axis',(0.,-1.,0.));
#7251=DIRECTION('ref_axis',(1.,0.,0.));
#7252=DIRECTION('',(0.707106781186548,0.707106781186547,8.65956056235493E-17));
#7253=DIRECTION('center_axis',(0.,-1.,0.));
#7254=DIRECTION('ref_axis',(1.,0.,0.));
#7255=DIRECTION('center_axis',(0.,-1.,0.));
#7256=DIRECTION('ref_axis',(1.,0.,0.));
#7257=DIRECTION('',(0.,1.,0.));
#7258=DIRECTION('center_axis',(0.,1.,0.));
#7259=DIRECTION('ref_axis',(1.,0.,0.));
#7260=DIRECTION('center_axis',(0.,-1.,0.));
#7261=DIRECTION('ref_axis',(1.,0.,0.));
#7262=DIRECTION('',(-0.707106781186547,0.707106781186548,-8.65956056235493E-17));
#7263=DIRECTION('center_axis',(0.,-1.,0.));
#7264=DIRECTION('ref_axis',(0.,0.,-1.));
#7265=DIRECTION('center_axis',(0.,-1.,0.));
#7266=DIRECTION('ref_axis',(1.,0.,0.));
#7267=DIRECTION('center_axis',(0.,1.,0.));
#7268=DIRECTION('ref_axis',(1.,0.,0.));
#7269=DIRECTION('center_axis',(0.,1.,0.));
#7270=DIRECTION('ref_axis',(1.,0.,0.));
#7271=DIRECTION('',(-0.447213595499958,0.894427190999916,-5.47678698264203E-17));
#7272=DIRECTION('center_axis',(0.,-1.,0.));
#7273=DIRECTION('ref_axis',(1.,0.,0.));
#7274=DIRECTION('center_axis',(0.,1.,0.));
#7275=DIRECTION('ref_axis',(1.,0.,0.));
#7276=DIRECTION('',(0.,1.,0.));
#7277=DIRECTION('center_axis',(0.,1.,0.));
#7278=DIRECTION('ref_axis',(1.,0.,0.));
#7279=DIRECTION('center_axis',(0.,-1.,0.));
#7280=DIRECTION('ref_axis',(1.,0.,0.));
#7281=DIRECTION('',(-0.707106781186547,0.707106781186548,-8.65956056235493E-17));
#7282=DIRECTION('center_axis',(0.,-1.,0.));
#7283=DIRECTION('ref_axis',(0.,0.,-1.));
#7284=DIRECTION('center_axis',(0.866025403784439,0.,-0.5));
#7285=DIRECTION('ref_axis',(0.5,0.,0.866025403784439));
#7286=DIRECTION('',(-0.5,0.,-0.866025403784439));
#7287=DIRECTION('',(0.,-1.,0.));
#7288=DIRECTION('',(0.5,0.,0.866025403784439));
#7289=DIRECTION('',(0.,-1.,0.));
#7290=DIRECTION('center_axis',(1.20185167898973E-16,0.,-1.));
#7291=DIRECTION('ref_axis',(1.,0.,1.20185167898973E-16));
#7292=DIRECTION('',(-1.,0.,-1.20185167898973E-16));
#7293=DIRECTION('',(0.,-1.,0.));
#7294=DIRECTION('',(1.,0.,1.20185167898973E-16));
#7295=DIRECTION('center_axis',(-0.866025403784439,0.,-0.5));
#7296=DIRECTION('ref_axis',(0.5,0.,-0.866025403784439));
#7297=DIRECTION('',(-0.5,0.,0.866025403784439));
#7298=DIRECTION('',(0.,-1.,0.));
#7299=DIRECTION('',(0.5,0.,-0.866025403784439));
#7300=DIRECTION('center_axis',(-0.866025403784439,0.,0.5));
#7301=DIRECTION('ref_axis',(-0.5,0.,-0.866025403784439));
#7302=DIRECTION('',(0.5,0.,0.866025403784439));
#7303=DIRECTION('',(0.,-1.,0.));
#7304=DIRECTION('',(-0.5,0.,-0.866025403784439));
#7305=DIRECTION('center_axis',(-2.40370335797945E-16,0.,1.));
#7306=DIRECTION('ref_axis',(-1.,0.,-2.40370335797945E-16));
#7307=DIRECTION('',(1.,0.,2.40370335797945E-16));
#7308=DIRECTION('',(0.,-1.,0.));
#7309=DIRECTION('',(-1.,0.,-2.40370335797945E-16));
#7310=DIRECTION('center_axis',(0.866025403784439,0.,0.5));
#7311=DIRECTION('ref_axis',(-0.5,0.,0.866025403784439));
#7312=DIRECTION('',(0.5,0.,-0.866025403784439));
#7313=DIRECTION('',(-0.5,0.,0.866025403784439));
#7314=DIRECTION('center_axis',(0.,1.,0.));
#7315=DIRECTION('ref_axis',(1.,0.,0.));
#7316=DIRECTION('center_axis',(0.,-1.,0.));
#7317=DIRECTION('ref_axis',(0.,0.,-1.));
#9062=CARTESIAN_POINT('',(0.,0.,0.));
#9063=CARTESIAN_POINT('Origin',(0.375,0.5,0.));
#9064=CARTESIAN_POINT('',(-0.375,0.5,-4.59242549680257E-17));
#9065=CARTESIAN_POINT('Origin',(0.,0.5,0.));
#9066=CARTESIAN_POINT('Origin',(0.,0.475,0.));
#9067=CARTESIAN_POINT('',(-0.425,0.45,-5.20474889637625E-17));
#9068=CARTESIAN_POINT('Origin',(0.,0.45,0.));
#9069=CARTESIAN_POINT('',(-0.4,0.475,-4.89858719658941E-17));
#9070=CARTESIAN_POINT('Origin',(0.,0.24,0.));
#9071=CARTESIAN_POINT('',(-0.425,0.0299999999999998,-5.20474889637625E-17));
#9072=CARTESIAN_POINT('Origin',(0.,0.0299999999999998,0.));
#9073=CARTESIAN_POINT('',(-0.425,0.24,-5.20474889637625E-17));
#9074=CARTESIAN_POINT('Origin',(0.,0.0150000000000001,0.));
#9075=CARTESIAN_POINT('',(-0.395,4.85722573273506E-17,-4.83735485663204E-17));
#9076=CARTESIAN_POINT('Origin',(0.,0.,0.));
#9077=CARTESIAN_POINT('',(-0.41,0.0150000000000001,-5.02105187650415E-17));
#9078=CARTESIAN_POINT('Origin',(0.27,0.,0.));
#9079=CARTESIAN_POINT('',(-0.27,0.,-3.30654635769785E-17));
#9080=CARTESIAN_POINT('Origin',(0.,0.,0.));
#9081=CARTESIAN_POINT('Origin',(0.,-0.02,0.));
#9082=CARTESIAN_POINT('',(-0.24505,-0.0498999999999999,3.00099698131059E-17));
#9083=CARTESIAN_POINT('Origin',(0.,-0.0498999999999999,0.));
#9084=CARTESIAN_POINT('',(-0.26,-0.02,-3.18408167778312E-17));
#9085=CARTESIAN_POINT('Origin',(0.,-0.995,0.));
#9086=CARTESIAN_POINT('',(-0.24505,-1.95495,3.00099698131059E-17));
#9087=CARTESIAN_POINT('Origin',(0.,-1.95495,0.));
#9088=CARTESIAN_POINT('',(-0.24505,-0.995,-3.00099698131059E-17));
#9089=CARTESIAN_POINT('Origin',(0.,-1.975,0.));
#9090=CARTESIAN_POINT('',(-0.2,-2.,-2.44929359829471E-17));
#9091=CARTESIAN_POINT('Origin',(0.,-2.,0.));
#9092=CARTESIAN_POINT('',(-0.225,-1.975,-2.75545529808154E-17));
#9093=CARTESIAN_POINT('Origin',(0.,-2.,0.));
#9094=CARTESIAN_POINT('Origin',(0.115470053837925,-0.5,-0.2));
#9095=CARTESIAN_POINT('',(0.23094010767585,-0.5,0.));
#9096=CARTESIAN_POINT('',(0.115470053837925,-0.5,-0.2));
#9097=CARTESIAN_POINT('',(0.23094010767585,-0.5,0.));
#9098=CARTESIAN_POINT('',(0.115470053837925,-0.8,-0.2));
#9099=CARTESIAN_POINT('',(0.115470053837925,-0.5,-0.2));
#9100=CARTESIAN_POINT('',(0.23094010767585,-0.8,0.));
#9101=CARTESIAN_POINT('',(0.23094010767585,-0.8,0.));
#9102=CARTESIAN_POINT('',(0.23094010767585,-0.5,0.));
#9103=CARTESIAN_POINT('Origin',(-0.115470053837925,-0.5,-0.2));
#9104=CARTESIAN_POINT('',(-0.115470053837925,-0.5,-0.2));
#9105=CARTESIAN_POINT('',(0.115470053837925,-0.5,-0.2));
#9106=CARTESIAN_POINT('',(-0.115470053837925,-0.8,-0.2));
#9107=CARTESIAN_POINT('',(-0.115470053837925,-0.5,-0.2));
#9108=CARTESIAN_POINT('',(0.115470053837925,-0.8,-0.2));
#9109=CARTESIAN_POINT('Origin',(-0.23094010767585,-0.5,-2.77555756156289E-17));
#9110=CARTESIAN_POINT('',(-0.23094010767585,-0.5,-2.82820063659975E-17));
#9111=CARTESIAN_POINT('',(-0.115470053837925,-0.5,-0.2));
#9112=CARTESIAN_POINT('',(-0.23094010767585,-0.8,-2.77555756156289E-17));
#9113=CARTESIAN_POINT('',(-0.23094010767585,-0.5,-2.82820063659975E-17));
#9114=CARTESIAN_POINT('',(-0.115470053837925,-0.8,-0.2));
#9115=CARTESIAN_POINT('Origin',(-0.115470053837925,-0.5,0.2));
#9116=CARTESIAN_POINT('',(-0.115470053837925,-0.5,0.2));
#9117=CARTESIAN_POINT('',(-0.23094010767585,-0.5,-2.82820063659975E-17));
#9118=CARTESIAN_POINT('',(-0.115470053837925,-0.8,0.2));
#9119=CARTESIAN_POINT('',(-0.115470053837925,-0.5,0.2));
#9120=CARTESIAN_POINT('',(-0.23094010767585,-0.8,-2.82820063659975E-17));
#9121=CARTESIAN_POINT('Origin',(0.115470053837925,-0.5,0.2));
#9122=CARTESIAN_POINT('',(0.115470053837925,-0.5,0.2));
#9123=CARTESIAN_POINT('',(-0.115470053837925,-0.5,0.2));
#9124=CARTESIAN_POINT('',(0.115470053837925,-0.8,0.2));
#9125=CARTESIAN_POINT('',(0.115470053837925,-0.5,0.2));
#9126=CARTESIAN_POINT('',(-0.115470053837925,-0.8,0.2));
#9127=CARTESIAN_POINT('Origin',(0.23094010767585,-0.5,0.));
#9128=CARTESIAN_POINT('',(0.115470053837925,-0.5,0.2));
#9129=CARTESIAN_POINT('',(0.115470053837925,-0.8,0.2));
#9130=CARTESIAN_POINT('Origin',(0.,-0.5,0.));
#9131=CARTESIAN_POINT('Origin',(0.,-0.8,0.));
#10785=UNCERTAINTY_MEASURE_WITH_UNIT(LENGTH_MEASURE(0.001),#10838,
'DISTANCE_ACCURACY_VALUE',
'Maximum model space distance between geometric entities at asserted c
onnectivities');
#10807=UNCERTAINTY_MEASURE_WITH_UNIT(LENGTH_MEASURE(0.001),#10838,
'DISTANCE_ACCURACY_VALUE',
'Maximum model space distance between geometric entities at asserted c
onnectivities');
#10815=(
GEOMETRIC_REPRESENTATION_CONTEXT(3)
GLOBAL_UNCERTAINTY_ASSIGNED_CONTEXT((#10785))
GLOBAL_UNIT_ASSIGNED_CONTEXT((#10838,#10840,#10841))
REPRESENTATION_CONTEXT('','3D')
);
#10837=(
GEOMETRIC_REPRESENTATION_CONTEXT(3)
GLOBAL_UNCERTAINTY_ASSIGNED_CONTEXT((#10807))
GLOBAL_UNIT_ASSIGNED_CONTEXT((#10838,#10840,#10841))
REPRESENTATION_CONTEXT('','3D')
);
#10838=(
LENGTH_UNIT()
NAMED_UNIT(*)
SI_UNIT(.CENTI.,.METRE.)
);
#10840=(
NAMED_UNIT(*)
PLANE_ANGLE_UNIT()
SI_UNIT($,.RADIAN.)
);
#10841=(
NAMED_UNIT(*)
SI_UNIT($,.STERADIAN.)
SOLID_ANGLE_UNIT()
);
#10849=SHAPE_DEFINITION_REPRESENTATION(#10878,#10948);
#10878=PRODUCT_DEFINITION_SHAPE('',$,#10978);
#10948=SHAPE_REPRESENTATION('',(#6162),#10815);
#10970=PRODUCT_DEFINITION_CONTEXT('part definition',#11059,'design');
#10978=PRODUCT_DEFINITION('Cap Screw - M5x20','Cap Screw - M5x20',#11007,
#10970);
#11007=PRODUCT_DEFINITION_FORMATION('',$,#11068);
#11059=APPLICATION_CONTEXT(
'Core Data for Automotive Mechanical Design Process');
#11060=PRODUCT_CONTEXT('part definition',#11059,'mechanical');
#11068=PRODUCT('Cap Screw - M5x20','Cap Screw - M5x20',
'Cap Screw - M5x20',(#11060));
#11167=COLOUR_RGB('Black',0.12,0.14,0.17);
#11168=FILL_AREA_STYLE_COLOUR('',#11167);
#11169=FILL_AREA_STYLE('',(#11168));
#11170=SURFACE_STYLE_FILL_AREA(#11169);
#11171=SURFACE_SIDE_STYLE('',(#11170));
#11172=SURFACE_STYLE_USAGE(.BOTH.,#11171);
#11173=PRESENTATION_STYLE_ASSIGNMENT((#11172));
ENDSEC;
END-ISO-10303-21;
